ISO-10303-21;
HEADER;
/* Generated by software containing ST-Developer
 * from STEP Tools, Inc. (www.steptools.com) 
 */

FILE_DESCRIPTION(
/* description */ ('PAT-122'),
/* implementation_level */ '2;1');

FILE_NAME(
/* name */ 'Flat Washer - M5.step',
/* time_stamp */ '2026-10-29T20:20:12-07:00',
/* author */ (''),
/* organization */ (''),
/* preprocessor_version */ 'ST-DEVELOPER v20.2',
/* originating_system */ 'Autodesk Translation Framework v15.17.0.0',
/* authorisation */ '');

FILE_SCHEMA (('AUTOMOTIVE_DESIGN { 1 0 10303 214 3 1 1 }'));
ENDSEC;

DATA;
#10=MECHANICAL_DESIGN_GEOMETRIC_PRESENTATION_REPRESENTATION('',(#509),#10019);
#408=CONICAL_SURFACE('',#6258,0.275,0.785398163397449);
#465=SHAPE_REPRESENTATION_RELATIONSHIP('SRR','None',#10186,#487);
#487=ADVANCED_BREP_SHAPE_REPRESENTATION('',(#529),#10015);
#509=STYLED_ITEM('',(#10355),#529);
#529=MANIFOLD_SOLID_BREP('Body1',#5633);
#603=FACE_BOUND('',#1441,.T.);
#604=FACE_BOUND('',#1444,.T.);
#799=PLANE('',#6263);
#800=PLANE('',#6267);
#1074=FACE_OUTER_BOUND('',#1438,.T.);
#1075=FACE_OUTER_BOUND('',#1439,.T.);
#1076=FACE_OUTER_BOUND('',#1440,.T.);
#1077=FACE_OUTER_BOUND('',#1442,.T.);
#1078=FACE_OUTER_BOUND('',#1443,.T.);
#1438=EDGE_LOOP('',(#5105,#5106,#5107,#5108));
#1439=EDGE_LOOP('',(#5109,#5110,#5111,#5112));
#1440=EDGE_LOOP('',(#5113));
#1441=EDGE_LOOP('',(#5114));
#1442=EDGE_LOOP('',(#5115,#5116,#5117,#5118));
#1443=EDGE_LOOP('',(#5119));
#1444=EDGE_LOOP('',(#5120));
#1978=LINE('',#9706,#2522);
#1979=LINE('',#9710,#2523);
#1980=LINE('',#9717,#2524);
#2522=VECTOR('',#7673,0.275);
#2523=VECTOR('',#7678,0.265);
#2524=VECTOR('',#7687,0.5);
#2680=CIRCLE('',#6259,0.285);
#2681=CIRCLE('',#6260,0.265);
#2682=CIRCLE('',#6262,0.265);
#2683=CIRCLE('',#6264,0.5);
#2684=CIRCLE('',#6266,0.5);
#3118=VERTEX_POINT('',#9703);
#3119=VERTEX_POINT('',#9705);
#3120=VERTEX_POINT('',#9709);
#3121=VERTEX_POINT('',#9713);
#3122=VERTEX_POINT('',#9716);
#3787=EDGE_CURVE('',#3118,#3118,#2680,.T.);
#3788=EDGE_CURVE('',#3118,#3119,#1978,.T.);
#3789=EDGE_CURVE('',#3119,#3119,#2681,.T.);
#3790=EDGE_CURVE('',#3119,#3120,#1979,.T.);
#3791=EDGE_CURVE('',#3120,#3120,#2682,.T.);
#3792=EDGE_CURVE('',#3121,#3121,#2683,.T.);
#3793=EDGE_CURVE('',#3121,#3122,#1980,.T.);
#3794=EDGE_CURVE('',#3122,#3122,#2684,.T.);
#5105=ORIENTED_EDGE('',*,*,#3787,.T.);
#5106=ORIENTED_EDGE('',*,*,#3788,.T.);
#5107=ORIENTED_EDGE('',*,*,#3789,.T.);
#5108=ORIENTED_EDGE('',*,*,#3788,.F.);
#5109=ORIENTED_EDGE('',*,*,#3789,.F.);
#5110=ORIENTED_EDGE('',*,*,#3790,.T.);
#5111=ORIENTED_EDGE('',*,*,#3791,.T.);
#5112=ORIENTED_EDGE('',*,*,#3790,.F.);
#5113=ORIENTED_EDGE('',*,*,#3792,.T.);
#5114=ORIENTED_EDGE('',*,*,#3787,.F.);
#5115=ORIENTED_EDGE('',*,*,#3792,.F.);
#5116=ORIENTED_EDGE('',*,*,#3793,.T.);
#5117=ORIENTED_EDGE('',*,*,#3794,.T.);
#5118=ORIENTED_EDGE('',*,*,#3793,.F.);
#5119=ORIENTED_EDGE('',*,*,#3794,.F.);
#5120=ORIENTED_EDGE('',*,*,#3791,.F.);
#5313=CYLINDRICAL_SURFACE('',#6261,0.265);
#5314=CYLINDRICAL_SURFACE('',#6265,0.5);
#5570=ADVANCED_FACE('',(#1074),#408,.F.);
#5571=ADVANCED_FACE('',(#1075),#5313,.F.);
#5572=ADVANCED_FACE('',(#1076,#603),#799,.T.);
#5573=ADVANCED_FACE('',(#1077),#5314,.T.);
#5574=ADVANCED_FACE('',(#1078,#604),#800,.F.);
#5633=CLOSED_SHELL('',(#5570,#5571,#5572,#5573,#5574));
#6257=AXIS2_PLACEMENT_3D('',#9701,#7667,#7668);
#6258=AXIS2_PLACEMENT_3D('',#9702,#7669,#7670);
#6259=AXIS2_PLACEMENT_3D('',#9704,#7671,#7672);
#6260=AXIS2_PLACEMENT_3D('',#9707,#7674,#7675);
#6261=AXIS2_PLACEMENT_3D('',#9708,#7676,#7677);
#6262=AXIS2_PLACEMENT_3D('',#9711,#7679,#7680);
#6263=AXIS2_PLACEMENT_3D('',#9712,#7681,#7682);
#6264=AXIS2_PLACEMENT_3D('',#9714,#7683,#7684);
#6265=AXIS2_PLACEMENT_3D('',#9715,#7685,#7686);
#6266=AXIS2_PLACEMENT_3D('',#9718,#7688,#7689);
#6267=AXIS2_PLACEMENT_3D('',#9719,#7690,#7691);
#7667=DIRECTION('axis',(0.,0.,1.));
#7668=DIRECTION('refdir',(1.,0.,0.));
#7669=DIRECTION('center_axis',(0.,1.,0.));
#7670=DIRECTION('ref_axis',(1.,0.,0.));
#7671=DIRECTION('center_axis',(0.,1.,0.));
#7672=DIRECTION('ref_axis',(1.,0.,0.));
#7673=DIRECTION('',(0.707106781186548,-0.707106781186547,-8.65956056235494E-17));
#7674=DIRECTION('center_axis',(0.,-1.,0.));
#7675=DIRECTION('ref_axis',(1.,0.,0.));
#7676=DIRECTION('center_axis',(0.,1.,0.));
#7677=DIRECTION('ref_axis',(1.,0.,0.));
#7678=DIRECTION('',(0.,-1.,0.));
#7679=DIRECTION('center_axis',(0.,-1.,0.));
#7680=DIRECTION('ref_axis',(1.,0.,0.));
#7681=DIRECTION('center_axis',(0.,1.,0.));
#7682=DIRECTION('ref_axis',(1.,0.,0.));
#7683=DIRECTION('center_axis',(0.,1.,0.));
#7684=DIRECTION('ref_axis',(1.,0.,0.));
#7685=DIRECTION('center_axis',(0.,1.,0.));
#7686=DIRECTION('ref_axis',(1.,0.,0.));
#7687=DIRECTION('',(0.,-1.,0.));
#7688=DIRECTION('center_axis',(0.,1.,0.));
#7689=DIRECTION('ref_axis',(1.,0.,0.));
#7690=DIRECTION('center_axis',(0.,1.,0.));
#7691=DIRECTION('ref_axis',(1.,0.,0.));
#9701=CARTESIAN_POINT('',(0.,0.,0.));
#9702=CARTESIAN_POINT('Origin',(0.,0.09,0.));
#9703=CARTESIAN_POINT('',(-0.285,0.1,3.49024337756996E-17));
#9704=CARTESIAN_POINT('Origin',(0.,0.1,0.));
#9705=CARTESIAN_POINT('',(-0.265,0.08,-3.24531401774049E-17));
#9706=CARTESIAN_POINT('',(-0.275,0.09,3.36777869765522E-17));
#9707=CARTESIAN_POINT('Origin',(0.,0.08,0.));
#9708=CARTESIAN_POINT('Origin',(0.,0.,0.));
#9709=CARTESIAN_POINT('',(-0.265,0.,3.24531401774049E-17));
#9710=CARTESIAN_POINT('',(-0.265,0.,3.24531401774049E-17));
#9711=CARTESIAN_POINT('Origin',(0.,0.,0.));
#9712=CARTESIAN_POINT('Origin',(0.,0.1,0.));
#9713=CARTESIAN_POINT('',(-0.5,0.1,6.12323399573677E-17));
#9714=CARTESIAN_POINT('Origin',(0.,0.1,0.));
#9715=CARTESIAN_POINT('Origin',(0.,0.,0.));
#9716=CARTESIAN_POINT('',(-0.5,0.,6.12323399573677E-17));
#9717=CARTESIAN_POINT('',(-0.5,0.,6.12323399573677E-17));
#9718=CARTESIAN_POINT('Origin',(0.,0.,0.));
#9719=CARTESIAN_POINT('Origin',(0.,0.,0.));
#9991=UNCERTAINTY_MEASURE_WITH_UNIT(LENGTH_MEASURE(0.001),#10020,
'DISTANCE_ACCURACY_VALUE',
'Maximum model space distance between geometric entities at asserted c
onnectivities');
#9995=UNCERTAINTY_MEASURE_WITH_UNIT(LENGTH_MEASURE(0.001),#10020,
'DISTANCE_ACCURACY_VALUE',
'Maximum model space distance between geometric entities at asserted c
onnectivities');
#10015=(
GEOMETRIC_REPRESENTATION_CONTEXT(3)
GLOBAL_UNCERTAINTY_ASSIGNED_CONTEXT((#9991))
GLOBAL_UNIT_ASSIGNED_CONTEXT((#10020,#10022,#10023))
REPRESENTATION_CONTEXT('','3D')
);
#10019=(
GEOMETRIC_REPRESENTATION_CONTEXT(3)
GLOBAL_UNCERTAINTY_ASSIGNED_CONTEXT((#9995))
GLOBAL_UNIT_ASSIGNED_CONTEXT((#10020,#10022,#10023))
REPRESENTATION_CONTEXT('','3D')
);
#10020=(
LENGTH_UNIT()
NAMED_UNIT(*)
SI_UNIT(.CENTI.,.METRE.)
);
#10022=(
NAMED_UNIT(*)
PLANE_ANGLE_UNIT()
SI_UNIT($,.RADIAN.)
);
#10023=(
NAMED_UNIT(*)
SI_UNIT($,.STERADIAN.)
SOLID_ANGLE_UNIT()
);
#10043=SHAPE_DEFINITION_REPRESENTATION(#10066,#10186);
#10066=PRODUCT_DEFINITION_SHAPE('',$,#10210);
#10186=SHAPE_REPRESENTATION('',(#6257),#10015);
#10190=PRODUCT_DEFINITION_CONTEXT('part definition',#10261,'design');
#10210=PRODUCT_DEFINITION('Flat Washer - M5',
'Flat Washer - M5',#10233,#10190);
#10233=PRODUCT_DEFINITION_FORMATION('',$,#10282);
#10261=APPLICATION_CONTEXT(
'Core Data for Automotive Mechanical Design Process');
#10262=PRODUCT_CONTEXT('part definition',#10261,'mechanical');
#10282=PRODUCT('Flat Washer - M5','Flat Washer - M5',
'Flat Washer - M5',(#10262));
#10349=COLOUR_RGB('Black',0.12,0.14,0.17);
#10350=FILL_AREA_STYLE_COLOUR('',#10349);
#10351=FILL_AREA_STYLE('',(#10350));
#10352=SURFACE_STYLE_FILL_AREA(#10351);
#10353=SURFACE_SIDE_STYLE('',(#10352));
#10354=SURFACE_STYLE_USAGE(.BOTH.,#10353);
#10355=PRESENTATION_STYLE_ASSIGNMENT((#10354));
ENDSEC;
END-ISO-10303-21;
